ISO-10303-21;
HEADER;
/* Generated by software containing ST-Developer
 * from STEP Tools, Inc. (www.steptools.com) 
 */

FILE_DESCRIPTION(
/* description */ ('Turntable on roller ring'),
/* implementation_level */ '2;1');

FILE_NAME(
/* name */ 'Roller bracket (2).step',
/* time_stamp */ '2026-10-28T03:23:59-07:00',
/* author */ (''),
/* organization */ (''),
/* preprocessor_version */ 'ST-DEVELOPER v20.2',
/* originating_system */ 'Autodesk Translation Framework v15.17.0.0',
/* authorisation */ '');

FILE_SCHEMA (('AUTOMOTIVE_DESIGN { 1 0 10303 214 3 1 1 }'));
ENDSEC;

DATA;
#10=MECHANICAL_DESIGN_GEOMETRIC_PRESENTATION_REPRESENTATION('',(#652),#16281);
#533=SHAPE_REPRESENTATION_RELATIONSHIP('SRR','None',#16552,#588);
#588=ADVANCED_BREP_SHAPE_REPRESENTATION('',(#722),#16246);
#652=STYLED_ITEM('',(#16911),#722);
#722=MANIFOLD_SOLID_BREP('Body1',#8395);
#911=FACE_BOUND('',#2211,.T.);
#912=FACE_BOUND('',#2213,.T.);
#913=FACE_BOUND('',#2218,.T.);
#914=FACE_BOUND('',#2220,.T.);
#915=FACE_BOUND('',#2226,.T.);
#916=FACE_BOUND('',#2227,.T.);
#917=FACE_BOUND('',#2228,.T.);
#918=FACE_BOUND('',#2229,.T.);
#919=FACE_BOUND('',#2230,.T.);
#920=FACE_BOUND('',#2231,.T.);
#921=FACE_BOUND('',#2233,.T.);
#922=FACE_BOUND('',#2234,.T.);
#923=FACE_BOUND('',#2235,.T.);
#924=FACE_BOUND('',#2236,.T.);
#1135=PLANE('',#9706);
#1136=PLANE('',#9707);
#1137=PLANE('',#9708);
#1138=PLANE('',#9709);
#1139=PLANE('',#9710);
#1140=PLANE('',#9711);
#1141=PLANE('',#9712);
#1142=PLANE('',#9713);
#1143=PLANE('',#9714);
#1144=PLANE('',#9715);
#1145=PLANE('',#9716);
#1146=PLANE('',#9717);
#1147=PLANE('',#9718);
#1148=PLANE('',#9719);
#1149=PLANE('',#9720);
#1150=PLANE('',#9721);
#1542=FACE_OUTER_BOUND('',#2201,.T.);
#1543=FACE_OUTER_BOUND('',#2202,.T.);
#1544=FACE_OUTER_BOUND('',#2203,.T.);
#1545=FACE_OUTER_BOUND('',#2204,.T.);
#1546=FACE_OUTER_BOUND('',#2205,.T.);
#1547=FACE_OUTER_BOUND('',#2206,.T.);
#1548=FACE_OUTER_BOUND('',#2207,.T.);
#1549=FACE_OUTER_BOUND('',#2208,.T.);
#1550=FACE_OUTER_BOUND('',#2209,.T.);
#1551=FACE_OUTER_BOUND('',#2210,.T.);
#1552=FACE_OUTER_BOUND('',#2212,.T.);
#1553=FACE_OUTER_BOUND('',#2214,.T.);
#1554=FACE_OUTER_BOUND('',#2215,.T.);
#1555=FACE_OUTER_BOUND('',#2216,.T.);
#1556=FACE_OUTER_BOUND('',#2217,.T.);
#1557=FACE_OUTER_BOUND('',#2219,.T.);
#1558=FACE_OUTER_BOUND('',#2221,.T.);
#1559=FACE_OUTER_BOUND('',#2222,.T.);
#1560=FACE_OUTER_BOUND('',#2223,.T.);
#1561=FACE_OUTER_BOUND('',#2224,.T.);
#1562=FACE_OUTER_BOUND('',#2225,.T.);
#1563=FACE_OUTER_BOUND('',#2232,.T.);
#2201=EDGE_LOOP('',(#6869,#6870,#6871,#6872));
#2202=EDGE_LOOP('',(#6873,#6874,#6875,#6876));
#2203=EDGE_LOOP('',(#6877,#6878,#6879,#6880));
#2204=EDGE_LOOP('',(#6881,#6882,#6883,#6884));
#2205=EDGE_LOOP('',(#6885,#6886,#6887,#6888));
#2206=EDGE_LOOP('',(#6889,#6890,#6891,#6892));
#2207=EDGE_LOOP('',(#6893,#6894,#6895,#6896));
#2208=EDGE_LOOP('',(#6897,#6898,#6899,#6900));
#2209=EDGE_LOOP('',(#6901,#6902,#6903,#6904));
#2210=EDGE_LOOP('',(#6905,#6906,#6907,#6908));
#2211=EDGE_LOOP('',(#6909));
#2212=EDGE_LOOP('',(#6910,#6911,#6912,#6913));
#2213=EDGE_LOOP('',(#6914));
#2214=EDGE_LOOP('',(#6915,#6916,#6917,#6918));
#2215=EDGE_LOOP('',(#6919,#6920,#6921,#6922));
#2216=EDGE_LOOP('',(#6923,#6924,#6925,#6926));
#2217=EDGE_LOOP('',(#6927,#6928,#6929,#6930));
#2218=EDGE_LOOP('',(#6931));
#2219=EDGE_LOOP('',(#6932,#6933,#6934,#6935));
#2220=EDGE_LOOP('',(#6936));
#2221=EDGE_LOOP('',(#6937,#6938,#6939,#6940));
#2222=EDGE_LOOP('',(#6941,#6942,#6943,#6944));
#2223=EDGE_LOOP('',(#6945,#6946,#6947,#6948));
#2224=EDGE_LOOP('',(#6949,#6950,#6951,#6952));
#2225=EDGE_LOOP('',(#6953,#6954,#6955,#6956));
#2226=EDGE_LOOP('',(#6957,#6958,#6959,#6960));
#2227=EDGE_LOOP('',(#6961,#6962,#6963,#6964));
#2228=EDGE_LOOP('',(#6965));
#2229=EDGE_LOOP('',(#6966));
#2230=EDGE_LOOP('',(#6967));
#2231=EDGE_LOOP('',(#6968));
#2232=EDGE_LOOP('',(#6969,#6970,#6971,#6972));
#2233=EDGE_LOOP('',(#6973));
#2234=EDGE_LOOP('',(#6974));
#2235=EDGE_LOOP('',(#6975));
#2236=EDGE_LOOP('',(#6976));
#2788=LINE('',#14818,#3271);
#2789=LINE('',#14824,#3272);
#2790=LINE('',#14830,#3273);
#2791=LINE('',#14836,#3274);
#2792=LINE('',#14842,#3275);
#2793=LINE('',#14848,#3276);
#2794=LINE('',#14853,#3277);
#2795=LINE('',#14855,#3278);
#2796=LINE('',#14857,#3279);
#2797=LINE('',#14858,#3280);
#2798=LINE('',#14862,#3281);
#2799=LINE('',#14864,#3282);
#2800=LINE('',#14866,#3283);
#2801=LINE('',#14867,#3284);
#2802=LINE('',#14869,#3285);
#2803=LINE('',#14870,#3286);
#2804=LINE('',#14872,#3287);
#2805=LINE('',#14874,#3288);
#2806=LINE('',#14878,#3289);
#2807=LINE('',#14880,#3290);
#2808=LINE('',#14882,#3291);
#2809=LINE('',#14883,#3292);
#2810=LINE('',#14887,#3293);
#2811=LINE('',#14889,#3294);
#2812=LINE('',#14891,#3295);
#2813=LINE('',#14892,#3296);
#2814=LINE('',#14894,#3297);
#2815=LINE('',#14895,#3298);
#2816=LINE('',#14897,#3299);
#2817=LINE('',#14899,#3300);
#2818=LINE('',#14903,#3301);
#2819=LINE('',#14905,#3302);
#2820=LINE('',#14907,#3303);
#2821=LINE('',#14908,#3304);
#2822=LINE('',#14911,#3305);
#2823=LINE('',#14913,#3306);
#2824=LINE('',#14914,#3307);
#2825=LINE('',#14917,#3308);
#2826=LINE('',#14919,#3309);
#2827=LINE('',#14920,#3310);
#2828=LINE('',#14922,#3311);
#2829=LINE('',#14923,#3312);
#3271=VECTOR('',#11795,0.275);
#3272=VECTOR('',#11802,0.275);
#3273=VECTOR('',#11809,0.275);
#3274=VECTOR('',#11816,0.275);
#3275=VECTOR('',#11823,0.5);
#3276=VECTOR('',#11830,0.5);
#3277=VECTOR('',#11835,1.);
#3278=VECTOR('',#11836,1.);
#3279=VECTOR('',#11837,1.);
#3280=VECTOR('',#11838,1.);
#3281=VECTOR('',#11841,1.);
#3282=VECTOR('',#11842,1.);
#3283=VECTOR('',#11843,1.);
#3284=VECTOR('',#11844,1.);
#3285=VECTOR('',#11847,1.);
#3286=VECTOR('',#11848,1.);
#3287=VECTOR('',#11851,1.);
#3288=VECTOR('',#11854,1.);
#3289=VECTOR('',#11857,1.);
#3290=VECTOR('',#11858,1.);
#3291=VECTOR('',#11859,1.);
#3292=VECTOR('',#11860,1.);
#3293=VECTOR('',#11863,1.);
#3294=VECTOR('',#11864,1.);
#3295=VECTOR('',#11865,1.);
#3296=VECTOR('',#11866,1.);
#3297=VECTOR('',#11869,1.);
#3298=VECTOR('',#11870,1.);
#3299=VECTOR('',#11873,1.);
#3300=VECTOR('',#11876,1.);
#3301=VECTOR('',#11879,1.);
#3302=VECTOR('',#11880,1.);
#3303=VECTOR('',#11881,1.);
#3304=VECTOR('',#11882,1.);
#3305=VECTOR('',#11885,1.);
#3306=VECTOR('',#11886,1.);
#3307=VECTOR('',#11887,1.);
#3308=VECTOR('',#11890,1.);
#3309=VECTOR('',#11891,1.);
#3310=VECTOR('',#11892,1.);
#3311=VECTOR('',#11895,1.);
#3312=VECTOR('',#11896,1.);
#3755=CIRCLE('',#9689,0.275);
#3756=CIRCLE('',#9690,0.275);
#3757=CIRCLE('',#9692,0.275);
#3758=CIRCLE('',#9693,0.275);
#3759=CIRCLE('',#9695,0.275);
#3760=CIRCLE('',#9696,0.275);
#3761=CIRCLE('',#9698,0.275);
#3762=CIRCLE('',#9699,0.275);
#3763=CIRCLE('',#9701,0.5);
#3764=CIRCLE('',#9702,0.5);
#3765=CIRCLE('',#9704,0.5);
#3766=CIRCLE('',#9705,0.5);
#4359=VERTEX_POINT('',#14815);
#4360=VERTEX_POINT('',#14817);
#4361=VERTEX_POINT('',#14821);
#4362=VERTEX_POINT('',#14823);
#4363=VERTEX_POINT('',#14827);
#4364=VERTEX_POINT('',#14829);
#4365=VERTEX_POINT('',#14833);
#4366=VERTEX_POINT('',#14835);
#4367=VERTEX_POINT('',#14839);
#4368=VERTEX_POINT('',#14841);
#4369=VERTEX_POINT('',#14845);
#4370=VERTEX_POINT('',#14847);
#4371=VERTEX_POINT('',#14851);
#4372=VERTEX_POINT('',#14852);
#4373=VERTEX_POINT('',#14854);
#4374=VERTEX_POINT('',#14856);
#4375=VERTEX_POINT('',#14860);
#4376=VERTEX_POINT('',#14861);
#4377=VERTEX_POINT('',#14863);
#4378=VERTEX_POINT('',#14865);
#4379=VERTEX_POINT('',#14876);
#4380=VERTEX_POINT('',#14877);
#4381=VERTEX_POINT('',#14879);
#4382=VERTEX_POINT('',#14881);
#4383=VERTEX_POINT('',#14885);
#4384=VERTEX_POINT('',#14886);
#4385=VERTEX_POINT('',#14888);
#4386=VERTEX_POINT('',#14890);
#4387=VERTEX_POINT('',#14901);
#4388=VERTEX_POINT('',#14902);
#4389=VERTEX_POINT('',#14904);
#4390=VERTEX_POINT('',#14906);
#4391=VERTEX_POINT('',#14910);
#4392=VERTEX_POINT('',#14912);
#4393=VERTEX_POINT('',#14916);
#4394=VERTEX_POINT('',#14918);
#5245=EDGE_CURVE('',#4359,#4359,#3755,.T.);
#5246=EDGE_CURVE('',#4359,#4360,#2788,.T.);
#5247=EDGE_CURVE('',#4360,#4360,#3756,.T.);
#5248=EDGE_CURVE('',#4361,#4361,#3757,.T.);
#5249=EDGE_CURVE('',#4361,#4362,#2789,.T.);
#5250=EDGE_CURVE('',#4362,#4362,#3758,.T.);
#5251=EDGE_CURVE('',#4363,#4363,#3759,.T.);
#5252=EDGE_CURVE('',#4363,#4364,#2790,.T.);
#5253=EDGE_CURVE('',#4364,#4364,#3760,.T.);
#5254=EDGE_CURVE('',#4365,#4365,#3761,.T.);
#5255=EDGE_CURVE('',#4365,#4366,#2791,.T.);
#5256=EDGE_CURVE('',#4366,#4366,#3762,.T.);
#5257=EDGE_CURVE('',#4367,#4367,#3763,.T.);
#5258=EDGE_CURVE('',#4367,#4368,#2792,.T.);
#5259=EDGE_CURVE('',#4368,#4368,#3764,.T.);
#5260=EDGE_CURVE('',#4369,#4369,#3765,.T.);
#5261=EDGE_CURVE('',#4369,#4370,#2793,.T.);
#5262=EDGE_CURVE('',#4370,#4370,#3766,.T.);
#5263=EDGE_CURVE('',#4371,#4372,#2794,.T.);
#5264=EDGE_CURVE('',#4371,#4373,#2795,.T.);
#5265=EDGE_CURVE('',#4374,#4373,#2796,.T.);
#5266=EDGE_CURVE('',#4372,#4374,#2797,.T.);
#5267=EDGE_CURVE('',#4375,#4376,#2798,.T.);
#5268=EDGE_CURVE('',#4377,#4375,#2799,.T.);
#5269=EDGE_CURVE('',#4378,#4377,#2800,.T.);
#5270=EDGE_CURVE('',#4376,#4378,#2801,.T.);
#5271=EDGE_CURVE('',#4376,#4371,#2802,.T.);
#5272=EDGE_CURVE('',#4373,#4378,#2803,.T.);
#5273=EDGE_CURVE('',#4374,#4377,#2804,.T.);
#5274=EDGE_CURVE('',#4375,#4372,#2805,.T.);
#5275=EDGE_CURVE('',#4379,#4380,#2806,.T.);
#5276=EDGE_CURVE('',#4379,#4381,#2807,.T.);
#5277=EDGE_CURVE('',#4382,#4381,#2808,.T.);
#5278=EDGE_CURVE('',#4380,#4382,#2809,.T.);
#5279=EDGE_CURVE('',#4383,#4384,#2810,.T.);
#5280=EDGE_CURVE('',#4385,#4383,#2811,.T.);
#5281=EDGE_CURVE('',#4386,#4385,#2812,.T.);
#5282=EDGE_CURVE('',#4384,#4386,#2813,.T.);
#5283=EDGE_CURVE('',#4384,#4379,#2814,.T.);
#5284=EDGE_CURVE('',#4381,#4386,#2815,.T.);
#5285=EDGE_CURVE('',#4382,#4385,#2816,.T.);
#5286=EDGE_CURVE('',#4383,#4380,#2817,.T.);
#5287=EDGE_CURVE('',#4387,#4388,#2818,.T.);
#5288=EDGE_CURVE('',#4388,#4389,#2819,.T.);
#5289=EDGE_CURVE('',#4390,#4389,#2820,.T.);
#5290=EDGE_CURVE('',#4387,#4390,#2821,.T.);
#5291=EDGE_CURVE('',#4391,#4387,#2822,.T.);
#5292=EDGE_CURVE('',#4392,#4390,#2823,.T.);
#5293=EDGE_CURVE('',#4391,#4392,#2824,.T.);
#5294=EDGE_CURVE('',#4393,#4391,#2825,.T.);
#5295=EDGE_CURVE('',#4394,#4392,#2826,.T.);
#5296=EDGE_CURVE('',#4393,#4394,#2827,.T.);
#5297=EDGE_CURVE('',#4388,#4393,#2828,.T.);
#5298=EDGE_CURVE('',#4389,#4394,#2829,.T.);
#6869=ORIENTED_EDGE('',*,*,#5245,.F.);
#6870=ORIENTED_EDGE('',*,*,#5246,.T.);
#6871=ORIENTED_EDGE('',*,*,#5247,.F.);
#6872=ORIENTED_EDGE('',*,*,#5246,.F.);
#6873=ORIENTED_EDGE('',*,*,#5248,.F.);
#6874=ORIENTED_EDGE('',*,*,#5249,.T.);
#6875=ORIENTED_EDGE('',*,*,#5250,.F.);
#6876=ORIENTED_EDGE('',*,*,#5249,.F.);
#6877=ORIENTED_EDGE('',*,*,#5251,.F.);
#6878=ORIENTED_EDGE('',*,*,#5252,.T.);
#6879=ORIENTED_EDGE('',*,*,#5253,.F.);
#6880=ORIENTED_EDGE('',*,*,#5252,.F.);
#6881=ORIENTED_EDGE('',*,*,#5254,.F.);
#6882=ORIENTED_EDGE('',*,*,#5255,.T.);
#6883=ORIENTED_EDGE('',*,*,#5256,.F.);
#6884=ORIENTED_EDGE('',*,*,#5255,.F.);
#6885=ORIENTED_EDGE('',*,*,#5257,.F.);
#6886=ORIENTED_EDGE('',*,*,#5258,.T.);
#6887=ORIENTED_EDGE('',*,*,#5259,.F.);
#6888=ORIENTED_EDGE('',*,*,#5258,.F.);
#6889=ORIENTED_EDGE('',*,*,#5260,.F.);
#6890=ORIENTED_EDGE('',*,*,#5261,.T.);
#6891=ORIENTED_EDGE('',*,*,#5262,.F.);
#6892=ORIENTED_EDGE('',*,*,#5261,.F.);
#6893=ORIENTED_EDGE('',*,*,#5263,.F.);
#6894=ORIENTED_EDGE('',*,*,#5264,.T.);
#6895=ORIENTED_EDGE('',*,*,#5265,.F.);
#6896=ORIENTED_EDGE('',*,*,#5266,.F.);
#6897=ORIENTED_EDGE('',*,*,#5267,.F.);
#6898=ORIENTED_EDGE('',*,*,#5268,.F.);
#6899=ORIENTED_EDGE('',*,*,#5269,.F.);
#6900=ORIENTED_EDGE('',*,*,#5270,.F.);
#6901=ORIENTED_EDGE('',*,*,#5271,.F.);
#6902=ORIENTED_EDGE('',*,*,#5270,.T.);
#6903=ORIENTED_EDGE('',*,*,#5272,.F.);
#6904=ORIENTED_EDGE('',*,*,#5264,.F.);
#6905=ORIENTED_EDGE('',*,*,#5272,.T.);
#6906=ORIENTED_EDGE('',*,*,#5269,.T.);
#6907=ORIENTED_EDGE('',*,*,#5273,.F.);
#6908=ORIENTED_EDGE('',*,*,#5265,.T.);
#6909=ORIENTED_EDGE('',*,*,#5262,.T.);
#6910=ORIENTED_EDGE('',*,*,#5271,.T.);
#6911=ORIENTED_EDGE('',*,*,#5263,.T.);
#6912=ORIENTED_EDGE('',*,*,#5274,.F.);
#6913=ORIENTED_EDGE('',*,*,#5267,.T.);
#6914=ORIENTED_EDGE('',*,*,#5260,.T.);
#6915=ORIENTED_EDGE('',*,*,#5275,.F.);
#6916=ORIENTED_EDGE('',*,*,#5276,.T.);
#6917=ORIENTED_EDGE('',*,*,#5277,.F.);
#6918=ORIENTED_EDGE('',*,*,#5278,.F.);
#6919=ORIENTED_EDGE('',*,*,#5279,.F.);
#6920=ORIENTED_EDGE('',*,*,#5280,.F.);
#6921=ORIENTED_EDGE('',*,*,#5281,.F.);
#6922=ORIENTED_EDGE('',*,*,#5282,.F.);
#6923=ORIENTED_EDGE('',*,*,#5283,.F.);
#6924=ORIENTED_EDGE('',*,*,#5282,.T.);
#6925=ORIENTED_EDGE('',*,*,#5284,.F.);
#6926=ORIENTED_EDGE('',*,*,#5276,.F.);
#6927=ORIENTED_EDGE('',*,*,#5284,.T.);
#6928=ORIENTED_EDGE('',*,*,#5281,.T.);
#6929=ORIENTED_EDGE('',*,*,#5285,.F.);
#6930=ORIENTED_EDGE('',*,*,#5277,.T.);
#6931=ORIENTED_EDGE('',*,*,#5259,.T.);
#6932=ORIENTED_EDGE('',*,*,#5283,.T.);
#6933=ORIENTED_EDGE('',*,*,#5275,.T.);
#6934=ORIENTED_EDGE('',*,*,#5286,.F.);
#6935=ORIENTED_EDGE('',*,*,#5279,.T.);
#6936=ORIENTED_EDGE('',*,*,#5257,.T.);
#6937=ORIENTED_EDGE('',*,*,#5287,.T.);
#6938=ORIENTED_EDGE('',*,*,#5288,.T.);
#6939=ORIENTED_EDGE('',*,*,#5289,.F.);
#6940=ORIENTED_EDGE('',*,*,#5290,.F.);
#6941=ORIENTED_EDGE('',*,*,#5291,.T.);
#6942=ORIENTED_EDGE('',*,*,#5290,.T.);
#6943=ORIENTED_EDGE('',*,*,#5292,.F.);
#6944=ORIENTED_EDGE('',*,*,#5293,.F.);
#6945=ORIENTED_EDGE('',*,*,#5294,.T.);
#6946=ORIENTED_EDGE('',*,*,#5293,.T.);
#6947=ORIENTED_EDGE('',*,*,#5295,.F.);
#6948=ORIENTED_EDGE('',*,*,#5296,.F.);
#6949=ORIENTED_EDGE('',*,*,#5297,.T.);
#6950=ORIENTED_EDGE('',*,*,#5296,.T.);
#6951=ORIENTED_EDGE('',*,*,#5298,.F.);
#6952=ORIENTED_EDGE('',*,*,#5288,.F.);
#6953=ORIENTED_EDGE('',*,*,#5298,.T.);
#6954=ORIENTED_EDGE('',*,*,#5295,.T.);
#6955=ORIENTED_EDGE('',*,*,#5292,.T.);
#6956=ORIENTED_EDGE('',*,*,#5289,.T.);
#6957=ORIENTED_EDGE('',*,*,#5280,.T.);
#6958=ORIENTED_EDGE('',*,*,#5286,.T.);
#6959=ORIENTED_EDGE('',*,*,#5278,.T.);
#6960=ORIENTED_EDGE('',*,*,#5285,.T.);
#6961=ORIENTED_EDGE('',*,*,#5268,.T.);
#6962=ORIENTED_EDGE('',*,*,#5274,.T.);
#6963=ORIENTED_EDGE('',*,*,#5266,.T.);
#6964=ORIENTED_EDGE('',*,*,#5273,.T.);
#6965=ORIENTED_EDGE('',*,*,#5256,.T.);
#6966=ORIENTED_EDGE('',*,*,#5253,.T.);
#6967=ORIENTED_EDGE('',*,*,#5250,.T.);
#6968=ORIENTED_EDGE('',*,*,#5247,.T.);
#6969=ORIENTED_EDGE('',*,*,#5297,.F.);
#6970=ORIENTED_EDGE('',*,*,#5287,.F.);
#6971=ORIENTED_EDGE('',*,*,#5291,.F.);
#6972=ORIENTED_EDGE('',*,*,#5294,.F.);
#6973=ORIENTED_EDGE('',*,*,#5245,.T.);
#6974=ORIENTED_EDGE('',*,*,#5248,.T.);
#6975=ORIENTED_EDGE('',*,*,#5251,.T.);
#6976=ORIENTED_EDGE('',*,*,#5254,.T.);
#7783=CYLINDRICAL_SURFACE('',#9688,0.275);
#7784=CYLINDRICAL_SURFACE('',#9691,0.275);
#7785=CYLINDRICAL_SURFACE('',#9694,0.275);
#7786=CYLINDRICAL_SURFACE('',#9697,0.275);
#7787=CYLINDRICAL_SURFACE('',#9700,0.5);
#7788=CYLINDRICAL_SURFACE('',#9703,0.5);
#8145=ADVANCED_FACE('',(#1542),#7783,.F.);
#8146=ADVANCED_FACE('',(#1543),#7784,.F.);
#8147=ADVANCED_FACE('',(#1544),#7785,.F.);
#8148=ADVANCED_FACE('',(#1545),#7786,.F.);
#8149=ADVANCED_FACE('',(#1546),#7787,.F.);
#8150=ADVANCED_FACE('',(#1547),#7788,.F.);
#8151=ADVANCED_FACE('',(#1548),#1135,.T.);
#8152=ADVANCED_FACE('',(#1549),#1136,.T.);
#8153=ADVANCED_FACE('',(#1550),#1137,.T.);
#8154=ADVANCED_FACE('',(#1551,#911),#1138,.T.);
#8155=ADVANCED_FACE('',(#1552,#912),#1139,.F.);
#8156=ADVANCED_FACE('',(#1553),#1140,.T.);
#8157=ADVANCED_FACE('',(#1554),#1141,.T.);
#8158=ADVANCED_FACE('',(#1555),#1142,.T.);
#8159=ADVANCED_FACE('',(#1556,#913),#1143,.T.);
#8160=ADVANCED_FACE('',(#1557,#914),#1144,.F.);
#8161=ADVANCED_FACE('',(#1558),#1145,.T.);
#8162=ADVANCED_FACE('',(#1559),#1146,.T.);
#8163=ADVANCED_FACE('',(#1560),#1147,.T.);
#8164=ADVANCED_FACE('',(#1561),#1148,.T.);
#8165=ADVANCED_FACE('',(#1562,#915,#916,#917,#918,#919,#920),#1149,.T.);
#8166=ADVANCED_FACE('',(#1563,#921,#922,#923,#924),#1150,.F.);
#8395=CLOSED_SHELL('',(#8145,#8146,#8147,#8148,#8149,#8150,#8151,#8152,
#8153,#8154,#8155,#8156,#8157,#8158,#8159,#8160,#8161,#8162,#8163,#8164,
#8165,#8166));
#9687=AXIS2_PLACEMENT_3D('',#14813,#11789,#11790);
#9688=AXIS2_PLACEMENT_3D('',#14814,#11791,#11792);
#9689=AXIS2_PLACEMENT_3D('',#14816,#11793,#11794);
#9690=AXIS2_PLACEMENT_3D('',#14819,#11796,#11797);
#9691=AXIS2_PLACEMENT_3D('',#14820,#11798,#11799);
#9692=AXIS2_PLACEMENT_3D('',#14822,#11800,#11801);
#9693=AXIS2_PLACEMENT_3D('',#14825,#11803,#11804);
#9694=AXIS2_PLACEMENT_3D('',#14826,#11805,#11806);
#9695=AXIS2_PLACEMENT_3D('',#14828,#11807,#11808);
#9696=AXIS2_PLACEMENT_3D('',#14831,#11810,#11811);
#9697=AXIS2_PLACEMENT_3D('',#14832,#11812,#11813);
#9698=AXIS2_PLACEMENT_3D('',#14834,#11814,#11815);
#9699=AXIS2_PLACEMENT_3D('',#14837,#11817,#11818);
#9700=AXIS2_PLACEMENT_3D('',#14838,#11819,#11820);
#9701=AXIS2_PLACEMENT_3D('',#14840,#11821,#11822);
#9702=AXIS2_PLACEMENT_3D('',#14843,#11824,#11825);
#9703=AXIS2_PLACEMENT_3D('',#14844,#11826,#11827);
#9704=AXIS2_PLACEMENT_3D('',#14846,#11828,#11829);
#9705=AXIS2_PLACEMENT_3D('',#14849,#11831,#11832);
#9706=AXIS2_PLACEMENT_3D('',#14850,#11833,#11834);
#9707=AXIS2_PLACEMENT_3D('',#14859,#11839,#11840);
#9708=AXIS2_PLACEMENT_3D('',#14868,#11845,#11846);
#9709=AXIS2_PLACEMENT_3D('',#14871,#11849,#11850);
#9710=AXIS2_PLACEMENT_3D('',#14873,#11852,#11853);
#9711=AXIS2_PLACEMENT_3D('',#14875,#11855,#11856);
#9712=AXIS2_PLACEMENT_3D('',#14884,#11861,#11862);
#9713=AXIS2_PLACEMENT_3D('',#14893,#11867,#11868);
#9714=AXIS2_PLACEMENT_3D('',#14896,#11871,#11872);
#9715=AXIS2_PLACEMENT_3D('',#14898,#11874,#11875);
#9716=AXIS2_PLACEMENT_3D('',#14900,#11877,#11878);
#9717=AXIS2_PLACEMENT_3D('',#14909,#11883,#11884);
#9718=AXIS2_PLACEMENT_3D('',#14915,#11888,#11889);
#9719=AXIS2_PLACEMENT_3D('',#14921,#11893,#11894);
#9720=AXIS2_PLACEMENT_3D('',#14924,#11897,#11898);
#9721=AXIS2_PLACEMENT_3D('',#14925,#11899,#11900);
#11789=DIRECTION('axis',(0.,0.,1.));
#11790=DIRECTION('refdir',(1.,0.,0.));
#11791=DIRECTION('center_axis',(0.,0.,1.));
#11792=DIRECTION('ref_axis',(1.,0.,0.));
#11793=DIRECTION('center_axis',(0.,0.,1.));
#11794=DIRECTION('ref_axis',(1.,0.,0.));
#11795=DIRECTION('',(0.,0.,1.));
#11796=DIRECTION('center_axis',(0.,0.,-1.));
#11797=DIRECTION('ref_axis',(1.,0.,0.));
#11798=DIRECTION('center_axis',(0.,0.,1.));
#11799=DIRECTION('ref_axis',(1.,0.,0.));
#11800=DIRECTION('center_axis',(0.,0.,1.));
#11801=DIRECTION('ref_axis',(1.,0.,0.));
#11802=DIRECTION('',(0.,0.,1.));
#11803=DIRECTION('center_axis',(0.,0.,-1.));
#11804=DIRECTION('ref_axis',(1.,0.,0.));
#11805=DIRECTION('center_axis',(0.,0.,1.));
#11806=DIRECTION('ref_axis',(1.,0.,0.));
#11807=DIRECTION('center_axis',(0.,0.,1.));
#11808=DIRECTION('ref_axis',(1.,0.,0.));
#11809=DIRECTION('',(0.,0.,1.));
#11810=DIRECTION('center_axis',(0.,0.,-1.));
#11811=DIRECTION('ref_axis',(1.,0.,0.));
#11812=DIRECTION('center_axis',(0.,0.,1.));
#11813=DIRECTION('ref_axis',(1.,0.,0.));
#11814=DIRECTION('center_axis',(0.,0.,1.));
#11815=DIRECTION('ref_axis',(1.,0.,0.));
#11816=DIRECTION('',(0.,0.,1.));
#11817=DIRECTION('center_axis',(0.,0.,-1.));
#11818=DIRECTION('ref_axis',(1.,0.,0.));
#11819=DIRECTION('center_axis',(0.,1.,0.));
#11820=DIRECTION('ref_axis',(1.,0.,0.));
#11821=DIRECTION('center_axis',(0.,1.,0.));
#11822=DIRECTION('ref_axis',(1.,0.,0.));
#11823=DIRECTION('',(0.,1.,0.));
#11824=DIRECTION('center_axis',(0.,-1.,0.));
#11825=DIRECTION('ref_axis',(1.,0.,0.));
#11826=DIRECTION('center_axis',(0.,1.,0.));
#11827=DIRECTION('ref_axis',(1.,0.,0.));
#11828=DIRECTION('center_axis',(0.,1.,0.));
#11829=DIRECTION('ref_axis',(1.,0.,0.));
#11830=DIRECTION('',(0.,1.,0.));
#11831=DIRECTION('center_axis',(0.,-1.,0.));
#11832=DIRECTION('ref_axis',(1.,0.,0.));
#11833=DIRECTION('center_axis',(-1.,0.,0.));
#11834=DIRECTION('ref_axis',(0.,0.,1.));
#11835=DIRECTION('',(0.,0.,-1.));
#11836=DIRECTION('',(0.,1.,0.));
#11837=DIRECTION('',(0.,0.,1.));
#11838=DIRECTION('',(0.,1.,0.));
#11839=DIRECTION('center_axis',(1.,0.,0.));
#11840=DIRECTION('ref_axis',(0.,0.,-1.));
#11841=DIRECTION('',(0.,0.,1.));
#11842=DIRECTION('',(0.,-1.,0.));
#11843=DIRECTION('',(0.,0.,-1.));
#11844=DIRECTION('',(0.,1.,0.));
#11845=DIRECTION('center_axis',(0.,0.,1.));
#11846=DIRECTION('ref_axis',(1.,0.,0.));
#11847=DIRECTION('',(-1.,0.,0.));
#11848=DIRECTION('',(1.,0.,0.));
#11849=DIRECTION('center_axis',(0.,1.,0.));
#11850=DIRECTION('ref_axis',(0.,0.,1.));
#11851=DIRECTION('',(1.,0.,0.));
#11852=DIRECTION('center_axis',(0.,1.,0.));
#11853=DIRECTION('ref_axis',(1.,0.,0.));
#11854=DIRECTION('',(-1.,0.,0.));
#11855=DIRECTION('center_axis',(-1.,0.,0.));
#11856=DIRECTION('ref_axis',(0.,0.,1.));
#11857=DIRECTION('',(0.,0.,-1.));
#11858=DIRECTION('',(0.,1.,0.));
#11859=DIRECTION('',(0.,0.,1.));
#11860=DIRECTION('',(0.,1.,0.));
#11861=DIRECTION('center_axis',(1.,0.,0.));
#11862=DIRECTION('ref_axis',(0.,0.,-1.));
#11863=DIRECTION('',(0.,0.,1.));
#11864=DIRECTION('',(0.,-1.,0.));
#11865=DIRECTION('',(0.,0.,-1.));
#11866=DIRECTION('',(0.,1.,0.));
#11867=DIRECTION('center_axis',(0.,0.,1.));
#11868=DIRECTION('ref_axis',(1.,0.,0.));
#11869=DIRECTION('',(-1.,0.,0.));
#11870=DIRECTION('',(1.,0.,0.));
#11871=DIRECTION('center_axis',(0.,1.,0.));
#11872=DIRECTION('ref_axis',(0.,0.,1.));
#11873=DIRECTION('',(1.,0.,0.));
#11874=DIRECTION('center_axis',(0.,1.,0.));
#11875=DIRECTION('ref_axis',(1.,0.,0.));
#11876=DIRECTION('',(-1.,0.,0.));
#11877=DIRECTION('center_axis',(0.,1.,0.));
#11878=DIRECTION('ref_axis',(-1.,0.,0.));
#11879=DIRECTION('',(-1.,0.,0.));
#11880=DIRECTION('',(0.,0.,1.));
#11881=DIRECTION('',(-1.,0.,0.));
#11882=DIRECTION('',(0.,0.,1.));
#11883=DIRECTION('center_axis',(1.,0.,0.));
#11884=DIRECTION('ref_axis',(0.,1.,0.));
#11885=DIRECTION('',(0.,1.,0.));
#11886=DIRECTION('',(0.,1.,0.));
#11887=DIRECTION('',(0.,0.,1.));
#11888=DIRECTION('center_axis',(0.,-1.,0.));
#11889=DIRECTION('ref_axis',(1.,0.,0.));
#11890=DIRECTION('',(1.,0.,0.));
#11891=DIRECTION('',(1.,0.,0.));
#11892=DIRECTION('',(0.,0.,1.));
#11893=DIRECTION('center_axis',(-1.,0.,0.));
#11894=DIRECTION('ref_axis',(0.,-1.,0.));
#11895=DIRECTION('',(0.,-1.,0.));
#11896=DIRECTION('',(0.,-1.,0.));
#11897=DIRECTION('center_axis',(0.,0.,1.));
#11898=DIRECTION('ref_axis',(1.,0.,0.));
#11899=DIRECTION('center_axis',(0.,0.,1.));
#11900=DIRECTION('ref_axis',(1.,0.,0.));
#14813=CARTESIAN_POINT('',(0.,0.,0.));
#14814=CARTESIAN_POINT('Origin',(1.8,13.,0.9));
#14815=CARTESIAN_POINT('',(1.525,13.,1.));
#14816=CARTESIAN_POINT('Origin',(1.8,13.,1.));
#14817=CARTESIAN_POINT('',(1.525,13.,1.4));
#14818=CARTESIAN_POINT('',(1.525,13.,0.9));
#14819=CARTESIAN_POINT('Origin',(1.8,13.,1.4));
#14820=CARTESIAN_POINT('Origin',(-1.8,17.,0.9));
#14821=CARTESIAN_POINT('',(-2.075,17.,1.));
#14822=CARTESIAN_POINT('Origin',(-1.8,17.,1.));
#14823=CARTESIAN_POINT('',(-2.075,17.,1.4));
#14824=CARTESIAN_POINT('',(-2.075,17.,0.9));
#14825=CARTESIAN_POINT('Origin',(-1.8,17.,1.4));
#14826=CARTESIAN_POINT('Origin',(-1.8,13.,0.9));
#14827=CARTESIAN_POINT('',(-2.075,13.,1.));
#14828=CARTESIAN_POINT('Origin',(-1.8,13.,1.));
#14829=CARTESIAN_POINT('',(-2.075,13.,1.4));
#14830=CARTESIAN_POINT('',(-2.075,13.,0.9));
#14831=CARTESIAN_POINT('Origin',(-1.8,13.,1.4));
#14832=CARTESIAN_POINT('Origin',(1.8,17.,0.9));
#14833=CARTESIAN_POINT('',(1.525,17.,1.));
#14834=CARTESIAN_POINT('Origin',(1.8,17.,1.));
#14835=CARTESIAN_POINT('',(1.525,17.,1.4));
#14836=CARTESIAN_POINT('',(1.525,17.,0.9));
#14837=CARTESIAN_POINT('Origin',(1.8,17.,1.4));
#14838=CARTESIAN_POINT('Origin',(0.,13.6,3.5));
#14839=CARTESIAN_POINT('',(-0.5,13.7,3.5));
#14840=CARTESIAN_POINT('Origin',(0.,13.7,3.5));
#14841=CARTESIAN_POINT('',(-0.5,14.1,3.5));
#14842=CARTESIAN_POINT('',(-0.5,13.6,3.5));
#14843=CARTESIAN_POINT('Origin',(0.,14.1,3.5));
#14844=CARTESIAN_POINT('Origin',(0.,13.6,3.5));
#14845=CARTESIAN_POINT('',(-0.5,15.9,3.5));
#14846=CARTESIAN_POINT('Origin',(0.,15.9,3.5));
#14847=CARTESIAN_POINT('',(-0.5,16.3,3.5));
#14848=CARTESIAN_POINT('',(-0.5,13.6,3.5));
#14849=CARTESIAN_POINT('Origin',(0.,16.3,3.5));
#14850=CARTESIAN_POINT('Origin',(-1.8,15.9,1.4));
#14851=CARTESIAN_POINT('',(-1.8,15.9,4.5));
#14852=CARTESIAN_POINT('',(-1.8,15.9,1.4));
#14853=CARTESIAN_POINT('',(-1.8,15.9,4.5));
#14854=CARTESIAN_POINT('',(-1.8,16.3,4.5));
#14855=CARTESIAN_POINT('',(-1.8,15.9,4.5));
#14856=CARTESIAN_POINT('',(-1.8,16.3,1.4));
#14857=CARTESIAN_POINT('',(-1.8,16.3,4.5));
#14858=CARTESIAN_POINT('',(-1.8,15.45,1.4));
#14859=CARTESIAN_POINT('Origin',(1.8,15.9,4.5));
#14860=CARTESIAN_POINT('',(1.8,15.9,1.4));
#14861=CARTESIAN_POINT('',(1.8,15.9,4.5));
#14862=CARTESIAN_POINT('',(1.8,15.9,1.4));
#14863=CARTESIAN_POINT('',(1.8,16.3,1.4));
#14864=CARTESIAN_POINT('',(1.8,15.45,1.4));
#14865=CARTESIAN_POINT('',(1.8,16.3,4.5));
#14866=CARTESIAN_POINT('',(1.8,16.3,1.4));
#14867=CARTESIAN_POINT('',(1.8,15.9,4.5));
#14868=CARTESIAN_POINT('Origin',(-1.8,15.9,4.5));
#14869=CARTESIAN_POINT('',(1.8,15.9,4.5));
#14870=CARTESIAN_POINT('',(1.8,16.3,4.5));
#14871=CARTESIAN_POINT('Origin',(0.,16.3,2.95));
#14872=CARTESIAN_POINT('',(0.,16.3,1.4));
#14873=CARTESIAN_POINT('Origin',(0.,15.9,2.95));
#14874=CARTESIAN_POINT('',(0.,15.9,1.4));
#14875=CARTESIAN_POINT('Origin',(-1.8,13.7,1.4));
#14876=CARTESIAN_POINT('',(-1.8,13.7,4.5));
#14877=CARTESIAN_POINT('',(-1.8,13.7,1.4));
#14878=CARTESIAN_POINT('',(-1.8,13.7,4.5));
#14879=CARTESIAN_POINT('',(-1.8,14.1,4.5));
#14880=CARTESIAN_POINT('',(-1.8,13.7,4.5));
#14881=CARTESIAN_POINT('',(-1.8,14.1,1.4));
#14882=CARTESIAN_POINT('',(-1.8,14.1,4.5));
#14883=CARTESIAN_POINT('',(-1.8,14.35,1.4));
#14884=CARTESIAN_POINT('Origin',(1.8,13.7,4.5));
#14885=CARTESIAN_POINT('',(1.8,13.7,1.4));
#14886=CARTESIAN_POINT('',(1.8,13.7,4.5));
#14887=CARTESIAN_POINT('',(1.8,13.7,1.4));
#14888=CARTESIAN_POINT('',(1.8,14.1,1.4));
#14889=CARTESIAN_POINT('',(1.8,14.35,1.4));
#14890=CARTESIAN_POINT('',(1.8,14.1,4.5));
#14891=CARTESIAN_POINT('',(1.8,14.1,1.4));
#14892=CARTESIAN_POINT('',(1.8,13.7,4.5));
#14893=CARTESIAN_POINT('Origin',(-1.8,13.7,4.5));
#14894=CARTESIAN_POINT('',(1.8,13.7,4.5));
#14895=CARTESIAN_POINT('',(1.8,14.1,4.5));
#14896=CARTESIAN_POINT('Origin',(0.,14.1,2.95));
#14897=CARTESIAN_POINT('',(0.,14.1,1.4));
#14898=CARTESIAN_POINT('Origin',(0.,13.7,2.95));
#14899=CARTESIAN_POINT('',(0.,13.7,1.4));
#14900=CARTESIAN_POINT('Origin',(2.5,17.5,1.));
#14901=CARTESIAN_POINT('',(2.5,17.5,1.));
#14902=CARTESIAN_POINT('',(-2.5,17.5,1.));
#14903=CARTESIAN_POINT('',(2.5,17.5,1.));
#14904=CARTESIAN_POINT('',(-2.5,17.5,1.4));
#14905=CARTESIAN_POINT('',(-2.5,17.5,1.));
#14906=CARTESIAN_POINT('',(2.5,17.5,1.4));
#14907=CARTESIAN_POINT('',(2.5,17.5,1.4));
#14908=CARTESIAN_POINT('',(2.5,17.5,1.));
#14909=CARTESIAN_POINT('Origin',(2.5,12.5,1.));
#14910=CARTESIAN_POINT('',(2.5,12.5,1.));
#14911=CARTESIAN_POINT('',(2.5,12.5,1.));
#14912=CARTESIAN_POINT('',(2.5,12.5,1.4));
#14913=CARTESIAN_POINT('',(2.5,12.5,1.4));
#14914=CARTESIAN_POINT('',(2.5,12.5,1.));
#14915=CARTESIAN_POINT('Origin',(-2.5,12.5,1.));
#14916=CARTESIAN_POINT('',(-2.5,12.5,1.));
#14917=CARTESIAN_POINT('',(-2.5,12.5,1.));
#14918=CARTESIAN_POINT('',(-2.5,12.5,1.4));
#14919=CARTESIAN_POINT('',(-2.5,12.5,1.4));
#14920=CARTESIAN_POINT('',(-2.5,12.5,1.));
#14921=CARTESIAN_POINT('Origin',(-2.5,17.5,1.));
#14922=CARTESIAN_POINT('',(-2.5,17.5,1.));
#14923=CARTESIAN_POINT('',(-2.5,17.5,1.4));
#14924=CARTESIAN_POINT('Origin',(0.,15.,1.4));
#14925=CARTESIAN_POINT('Origin',(0.,15.,1.));
#16177=UNCERTAINTY_MEASURE_WITH_UNIT(LENGTH_MEASURE(0.001),#16282,
'DISTANCE_ACCURACY_VALUE',
'Maximum model space distance between geometric entities at asserted c
onnectivities');
#16212=UNCERTAINTY_MEASURE_WITH_UNIT(LENGTH_MEASURE(0.001),#16282,
'DISTANCE_ACCURACY_VALUE',
'Maximum model space distance between geometric entities at asserted c
onnectivities');
#16246=(
GEOMETRIC_REPRESENTATION_CONTEXT(3)
GLOBAL_UNCERTAINTY_ASSIGNED_CONTEXT((#16177))
GLOBAL_UNIT_ASSIGNED_CONTEXT((#16282,#16284,#16285))
REPRESENTATION_CONTEXT('','3D')
);
#16281=(
GEOMETRIC_REPRESENTATION_CONTEXT(3)
GLOBAL_UNCERTAINTY_ASSIGNED_CONTEXT((#16212))
GLOBAL_UNIT_ASSIGNED_CONTEXT((#16282,#16284,#16285))
REPRESENTATION_CONTEXT('','3D')
);
#16282=(
LENGTH_UNIT()
NAMED_UNIT(*)
SI_UNIT(.CENTI.,.METRE.)
);
#16284=(
NAMED_UNIT(*)
PLANE_ANGLE_UNIT()
SI_UNIT($,.RADIAN.)
);
#16285=(
NAMED_UNIT(*)
SI_UNIT($,.STERADIAN.)
SOLID_ANGLE_UNIT()
);
#16319=SHAPE_DEFINITION_REPRESENTATION(#16413,#16552);
#16413=PRODUCT_DEFINITION_SHAPE('',$,#16621);
#16552=SHAPE_REPRESENTATION('',(#9687),#16246);
#16587=PRODUCT_DEFINITION_CONTEXT('part definition',#16793,'design');
#16621=PRODUCT_DEFINITION('Roller bracket (2)','Roller bracket (2)',#16689,
#16587);
#16689=PRODUCT_DEFINITION_FORMATION('',$,#16828);
#16793=APPLICATION_CONTEXT(
'Core Data for Automotive Mechanical Design Process');
#16794=PRODUCT_CONTEXT('part definition',#16793,'mechanical');
#16828=PRODUCT('Roller bracket (2)','Roller bracket (2)','Roller bracket (2)',
(#16794));
#16905=COLOUR_RGB('Dark Blue',0.08,0.2,0.34);
#16906=FILL_AREA_STYLE_COLOUR('',#16905);
#16907=FILL_AREA_STYLE('',(#16906));
#16908=SURFACE_STYLE_FILL_AREA(#16907);
#16909=SURFACE_SIDE_STYLE('',(#16908));
#16910=SURFACE_STYLE_USAGE(.BOTH.,#16909);
#16911=PRESENTATION_STYLE_ASSIGNMENT((#16910));
ENDSEC;
END-ISO-10303-21;
